ISO-10303-21;
HEADER;
/* Generated by software containing ST-Developer
 * from STEP Tools, Inc. (www.steptools.com) 
 */

FILE_DESCRIPTION(
/* description */ ('Torsion-spring ratchet demonstrator'),
/* implementation_level */ '2;1');

FILE_NAME(
/* name */ 'M4x4 collar screw.step',
/* time_stamp */ '2026-10-29T17:29:17-07:00',
/* author */ (''),
/* organization */ (''),
/* preprocessor_version */ 'ST-DEVELOPER v20.2',
/* originating_system */ 'Autodesk Translation Framework v15.17.0.0',
/* authorisation */ '');

FILE_SCHEMA (('AUTOMOTIVE_DESIGN { 1 0 10303 214 3 1 1 }'));
ENDSEC;

DATA;
#10=MECHANICAL_DESIGN_GEOMETRIC_PRESENTATION_REPRESENTATION('',(#311),#11258);
#196=CONICAL_SURFACE('',#5944,0.185,0.785398163397449);
#255=SHAPE_REPRESENTATION_RELATIONSHIP('SRR','None',#11383,#279);
#279=ADVANCED_BREP_SHAPE_REPRESENTATION('',(#341),#11253);
#311=STYLED_ITEM('',(#11591),#341);
#341=MANIFOLD_SOLID_BREP('Body1',#5184);
#428=FACE_BOUND('',#1230,.T.);
#540=PLANE('',#5933);
#541=PLANE('',#5935);
#542=PLANE('',#5936);
#543=PLANE('',#5937);
#544=PLANE('',#5938);
#545=PLANE('',#5939);
#546=PLANE('',#5940);
#547=PLANE('',#5941);
#548=PLANE('',#5942);
#833=FACE_OUTER_BOUND('',#1221,.T.);
#834=FACE_OUTER_BOUND('',#1222,.T.);
#835=FACE_OUTER_BOUND('',#1223,.T.);
#836=FACE_OUTER_BOUND('',#1224,.T.);
#837=FACE_OUTER_BOUND('',#1225,.T.);
#838=FACE_OUTER_BOUND('',#1226,.T.);
#839=FACE_OUTER_BOUND('',#1227,.T.);
#840=FACE_OUTER_BOUND('',#1228,.T.);
#841=FACE_OUTER_BOUND('',#1229,.T.);
#842=FACE_OUTER_BOUND('',#1231,.T.);
#843=FACE_OUTER_BOUND('',#1232,.T.);
#1221=EDGE_LOOP('',(#4274));
#1222=EDGE_LOOP('',(#4275,#4276,#4277,#4278));
#1223=EDGE_LOOP('',(#4279,#4280,#4281,#4282));
#1224=EDGE_LOOP('',(#4283,#4284,#4285,#4286));
#1225=EDGE_LOOP('',(#4287,#4288,#4289,#4290));
#1226=EDGE_LOOP('',(#4291,#4292,#4293,#4294));
#1227=EDGE_LOOP('',(#4295,#4296,#4297,#4298));
#1228=EDGE_LOOP('',(#4299,#4300,#4301,#4302,#4303,#4304));
#1229=EDGE_LOOP('',(#4305));
#1230=EDGE_LOOP('',(#4306,#4307,#4308,#4309,#4310,#4311));
#1231=EDGE_LOOP('',(#4312,#4313,#4314,#4315));
#1232=EDGE_LOOP('',(#4316,#4317,#4318,#4319));
#1491=LINE('',#10630,#1874);
#1492=LINE('',#10632,#1875);
#1493=LINE('',#10634,#1876);
#1494=LINE('',#10635,#1877);
#1495=LINE('',#10638,#1878);
#1496=LINE('',#10640,#1879);
#1497=LINE('',#10641,#1880);
#1498=LINE('',#10644,#1881);
#1499=LINE('',#10646,#1882);
#1500=LINE('',#10647,#1883);
#1501=LINE('',#10650,#1884);
#1502=LINE('',#10652,#1885);
#1503=LINE('',#10653,#1886);
#1504=LINE('',#10656,#1887);
#1505=LINE('',#10658,#1888);
#1506=LINE('',#10659,#1889);
#1507=LINE('',#10661,#1890);
#1508=LINE('',#10662,#1891);
#1509=LINE('',#10670,#1892);
#1510=LINE('',#10672,#1893);
#1874=VECTOR('',#7198,1.);
#1875=VECTOR('',#7199,1.);
#1876=VECTOR('',#7200,1.);
#1877=VECTOR('',#7201,1.);
#1878=VECTOR('',#7204,1.);
#1879=VECTOR('',#7205,1.);
#1880=VECTOR('',#7206,1.);
#1881=VECTOR('',#7209,1.);
#1882=VECTOR('',#7210,1.);
#1883=VECTOR('',#7211,1.);
#1884=VECTOR('',#7214,1.);
#1885=VECTOR('',#7215,1.);
#1886=VECTOR('',#7216,1.);
#1887=VECTOR('',#7219,1.);
#1888=VECTOR('',#7220,1.);
#1889=VECTOR('',#7221,1.);
#1890=VECTOR('',#7224,1.);
#1891=VECTOR('',#7225,1.);
#1892=VECTOR('',#7236,0.185);
#1893=VECTOR('',#7239,0.2);
#2311=CIRCLE('',#5934,0.1954);
#2312=CIRCLE('',#5943,0.17);
#2313=CIRCLE('',#5945,0.1954);
#2620=VERTEX_POINT('',#10625);
#2621=VERTEX_POINT('',#10628);
#2622=VERTEX_POINT('',#10629);
#2623=VERTEX_POINT('',#10631);
#2624=VERTEX_POINT('',#10633);
#2625=VERTEX_POINT('',#10637);
#2626=VERTEX_POINT('',#10639);
#2627=VERTEX_POINT('',#10643);
#2628=VERTEX_POINT('',#10645);
#2629=VERTEX_POINT('',#10649);
#2630=VERTEX_POINT('',#10651);
#2631=VERTEX_POINT('',#10655);
#2632=VERTEX_POINT('',#10657);
#2633=VERTEX_POINT('',#10665);
#2634=VERTEX_POINT('',#10668);
#3197=EDGE_CURVE('',#2620,#2620,#2311,.T.);
#3198=EDGE_CURVE('',#2621,#2622,#1491,.T.);
#3199=EDGE_CURVE('',#2621,#2623,#1492,.T.);
#3200=EDGE_CURVE('',#2623,#2624,#1493,.T.);
#3201=EDGE_CURVE('',#2622,#2624,#1494,.T.);
#3202=EDGE_CURVE('',#2625,#2621,#1495,.T.);
#3203=EDGE_CURVE('',#2625,#2626,#1496,.T.);
#3204=EDGE_CURVE('',#2626,#2623,#1497,.T.);
#3205=EDGE_CURVE('',#2627,#2625,#1498,.T.);
#3206=EDGE_CURVE('',#2627,#2628,#1499,.T.);
#3207=EDGE_CURVE('',#2628,#2626,#1500,.T.);
#3208=EDGE_CURVE('',#2629,#2627,#1501,.T.);
#3209=EDGE_CURVE('',#2629,#2630,#1502,.T.);
#3210=EDGE_CURVE('',#2630,#2628,#1503,.T.);
#3211=EDGE_CURVE('',#2631,#2629,#1504,.T.);
#3212=EDGE_CURVE('',#2631,#2632,#1505,.T.);
#3213=EDGE_CURVE('',#2632,#2630,#1506,.T.);
#3214=EDGE_CURVE('',#2622,#2631,#1507,.T.);
#3215=EDGE_CURVE('',#2624,#2632,#1508,.T.);
#3216=EDGE_CURVE('',#2633,#2633,#2312,.T.);
#3217=EDGE_CURVE('',#2634,#2634,#2313,.T.);
#3218=EDGE_CURVE('',#2634,#2633,#1509,.T.);
#3219=EDGE_CURVE('',#2620,#2634,#1510,.T.);
#4274=ORIENTED_EDGE('',*,*,#3197,.F.);
#4275=ORIENTED_EDGE('',*,*,#3198,.F.);
#4276=ORIENTED_EDGE('',*,*,#3199,.T.);
#4277=ORIENTED_EDGE('',*,*,#3200,.T.);
#4278=ORIENTED_EDGE('',*,*,#3201,.F.);
#4279=ORIENTED_EDGE('',*,*,#3202,.F.);
#4280=ORIENTED_EDGE('',*,*,#3203,.T.);
#4281=ORIENTED_EDGE('',*,*,#3204,.T.);
#4282=ORIENTED_EDGE('',*,*,#3199,.F.);
#4283=ORIENTED_EDGE('',*,*,#3205,.F.);
#4284=ORIENTED_EDGE('',*,*,#3206,.T.);
#4285=ORIENTED_EDGE('',*,*,#3207,.T.);
#4286=ORIENTED_EDGE('',*,*,#3203,.F.);
#4287=ORIENTED_EDGE('',*,*,#3208,.F.);
#4288=ORIENTED_EDGE('',*,*,#3209,.T.);
#4289=ORIENTED_EDGE('',*,*,#3210,.T.);
#4290=ORIENTED_EDGE('',*,*,#3206,.F.);
#4291=ORIENTED_EDGE('',*,*,#3211,.F.);
#4292=ORIENTED_EDGE('',*,*,#3212,.T.);
#4293=ORIENTED_EDGE('',*,*,#3213,.T.);
#4294=ORIENTED_EDGE('',*,*,#3209,.F.);
#4295=ORIENTED_EDGE('',*,*,#3214,.F.);
#4296=ORIENTED_EDGE('',*,*,#3201,.T.);
#4297=ORIENTED_EDGE('',*,*,#3215,.T.);
#4298=ORIENTED_EDGE('',*,*,#3212,.F.);
#4299=ORIENTED_EDGE('',*,*,#3215,.F.);
#4300=ORIENTED_EDGE('',*,*,#3200,.F.);
#4301=ORIENTED_EDGE('',*,*,#3204,.F.);
#4302=ORIENTED_EDGE('',*,*,#3207,.F.);
#4303=ORIENTED_EDGE('',*,*,#3210,.F.);
#4304=ORIENTED_EDGE('',*,*,#3213,.F.);
#4305=ORIENTED_EDGE('',*,*,#3216,.F.);
#4306=ORIENTED_EDGE('',*,*,#3198,.T.);
#4307=ORIENTED_EDGE('',*,*,#3214,.T.);
#4308=ORIENTED_EDGE('',*,*,#3211,.T.);
#4309=ORIENTED_EDGE('',*,*,#3208,.T.);
#4310=ORIENTED_EDGE('',*,*,#3205,.T.);
#4311=ORIENTED_EDGE('',*,*,#3202,.T.);
#4312=ORIENTED_EDGE('',*,*,#3217,.F.);
#4313=ORIENTED_EDGE('',*,*,#3218,.T.);
#4314=ORIENTED_EDGE('',*,*,#3216,.T.);
#4315=ORIENTED_EDGE('',*,*,#3218,.F.);
#4316=ORIENTED_EDGE('',*,*,#3197,.T.);
#4317=ORIENTED_EDGE('',*,*,#3219,.T.);
#4318=ORIENTED_EDGE('',*,*,#3217,.T.);
#4319=ORIENTED_EDGE('',*,*,#3219,.F.);
#4840=CYLINDRICAL_SURFACE('',#5946,0.1954);
#5059=ADVANCED_FACE('',(#833),#540,.F.);
#5060=ADVANCED_FACE('',(#834),#541,.F.);
#5061=ADVANCED_FACE('',(#835),#542,.F.);
#5062=ADVANCED_FACE('',(#836),#543,.F.);
#5063=ADVANCED_FACE('',(#837),#544,.F.);
#5064=ADVANCED_FACE('',(#838),#545,.F.);
#5065=ADVANCED_FACE('',(#839),#546,.F.);
#5066=ADVANCED_FACE('',(#840),#547,.F.);
#5067=ADVANCED_FACE('',(#841,#428),#548,.T.);
#5068=ADVANCED_FACE('',(#842),#196,.T.);
#5069=ADVANCED_FACE('',(#843),#4840,.T.);
#5184=CLOSED_SHELL('',(#5059,#5060,#5061,#5062,#5063,#5064,#5065,#5066,
#5067,#5068,#5069));
#5932=AXIS2_PLACEMENT_3D('',#10623,#7190,#7191);
#5933=AXIS2_PLACEMENT_3D('',#10624,#7192,#7193);
#5934=AXIS2_PLACEMENT_3D('',#10626,#7194,#7195);
#5935=AXIS2_PLACEMENT_3D('',#10627,#7196,#7197);
#5936=AXIS2_PLACEMENT_3D('',#10636,#7202,#7203);
#5937=AXIS2_PLACEMENT_3D('',#10642,#7207,#7208);
#5938=AXIS2_PLACEMENT_3D('',#10648,#7212,#7213);
#5939=AXIS2_PLACEMENT_3D('',#10654,#7217,#7218);
#5940=AXIS2_PLACEMENT_3D('',#10660,#7222,#7223);
#5941=AXIS2_PLACEMENT_3D('',#10663,#7226,#7227);
#5942=AXIS2_PLACEMENT_3D('',#10664,#7228,#7229);
#5943=AXIS2_PLACEMENT_3D('',#10666,#7230,#7231);
#5944=AXIS2_PLACEMENT_3D('',#10667,#7232,#7233);
#5945=AXIS2_PLACEMENT_3D('',#10669,#7234,#7235);
#5946=AXIS2_PLACEMENT_3D('',#10671,#7237,#7238);
#7190=DIRECTION('axis',(0.,0.,1.));
#7191=DIRECTION('refdir',(1.,0.,0.));
#7192=DIRECTION('center_axis',(0.,1.,0.));
#7193=DIRECTION('ref_axis',(1.,0.,0.));
#7194=DIRECTION('center_axis',(0.,1.,0.));
#7195=DIRECTION('ref_axis',(1.,0.,0.));
#7196=DIRECTION('center_axis',(0.866025403784439,0.,-0.5));
#7197=DIRECTION('ref_axis',(0.5,0.,0.866025403784439));
#7198=DIRECTION('',(0.5,0.,0.866025403784439));
#7199=DIRECTION('',(0.,-1.,0.));
#7200=DIRECTION('',(0.5,0.,0.866025403784439));
#7201=DIRECTION('',(0.,-1.,0.));
#7202=DIRECTION('center_axis',(1.20185167898973E-16,0.,-1.));
#7203=DIRECTION('ref_axis',(1.,0.,1.20185167898973E-16));
#7204=DIRECTION('',(1.,0.,1.20185167898973E-16));
#7205=DIRECTION('',(0.,-1.,0.));
#7206=DIRECTION('',(1.,0.,1.20185167898973E-16));
#7207=DIRECTION('center_axis',(-0.866025403784439,0.,-0.5));
#7208=DIRECTION('ref_axis',(0.5,0.,-0.866025403784439));
#7209=DIRECTION('',(0.5,0.,-0.866025403784439));
#7210=DIRECTION('',(0.,-1.,0.));
#7211=DIRECTION('',(0.5,0.,-0.866025403784439));
#7212=DIRECTION('center_axis',(-0.866025403784439,0.,0.5));
#7213=DIRECTION('ref_axis',(-0.5,0.,-0.866025403784439));
#7214=DIRECTION('',(-0.5,0.,-0.866025403784439));
#7215=DIRECTION('',(0.,-1.,0.));
#7216=DIRECTION('',(-0.5,0.,-0.866025403784439));
#7217=DIRECTION('center_axis',(-2.40370335797945E-16,0.,1.));
#7218=DIRECTION('ref_axis',(-1.,0.,-2.40370335797945E-16));
#7219=DIRECTION('',(-1.,0.,-2.40370335797945E-16));
#7220=DIRECTION('',(0.,-1.,0.));
#7221=DIRECTION('',(-1.,0.,-2.40370335797945E-16));
#7222=DIRECTION('center_axis',(0.866025403784439,0.,0.5));
#7223=DIRECTION('ref_axis',(-0.5,0.,0.866025403784439));
#7224=DIRECTION('',(-0.5,0.,0.866025403784439));
#7225=DIRECTION('',(-0.5,0.,0.866025403784439));
#7226=DIRECTION('center_axis',(0.,-1.,0.));
#7227=DIRECTION('ref_axis',(0.,0.,-1.));
#7228=DIRECTION('center_axis',(0.,1.,0.));
#7229=DIRECTION('ref_axis',(0.,0.,1.));
#7230=DIRECTION('center_axis',(0.,-1.,0.));
#7231=DIRECTION('ref_axis',(1.,0.,0.));
#7232=DIRECTION('center_axis',(0.,-1.,0.));
#7233=DIRECTION('ref_axis',(1.,0.,0.));
#7234=DIRECTION('center_axis',(0.,-1.,0.));
#7235=DIRECTION('ref_axis',(1.,0.,0.));
#7236=DIRECTION('',(0.707106781186548,0.707106781186547,8.65956056235494E-17));
#7237=DIRECTION('center_axis',(0.,-1.,0.));
#7238=DIRECTION('ref_axis',(1.,0.,0.));
#7239=DIRECTION('',(0.,1.,0.));
#10623=CARTESIAN_POINT('',(0.,0.,0.));
#10624=CARTESIAN_POINT('Origin',(0.,-0.4,0.));
#10625=CARTESIAN_POINT('',(-0.1954,-0.4,2.39295984553393E-17));
#10626=CARTESIAN_POINT('Origin',(0.,-0.4,0.));
#10627=CARTESIAN_POINT('Origin',(0.0577350269189626,0.,-0.1));
#10628=CARTESIAN_POINT('',(0.0577350269189626,0.,-0.1));
#10629=CARTESIAN_POINT('',(0.115470053837925,0.,0.));
#10630=CARTESIAN_POINT('',(0.0934187836487032,0.,-0.0381939203391614));
#10631=CARTESIAN_POINT('',(0.0577350269189626,-0.2,-0.1));
#10632=CARTESIAN_POINT('',(0.0577350269189626,0.,-0.1));
#10633=CARTESIAN_POINT('',(0.115470053837925,-0.2,0.));
#10634=CARTESIAN_POINT('',(0.115470053837925,-0.2,0.));
#10635=CARTESIAN_POINT('',(0.115470053837925,0.,0.));
#10636=CARTESIAN_POINT('Origin',(-0.0577350269189626,0.,-0.1));
#10637=CARTESIAN_POINT('',(-0.0577350269189626,0.,-0.1));
#10638=CARTESIAN_POINT('',(0.0561324865405187,0.,-0.1));
#10639=CARTESIAN_POINT('',(-0.0577350269189626,-0.2,-0.1));
#10640=CARTESIAN_POINT('',(-0.0577350269189626,0.,-0.1));
#10641=CARTESIAN_POINT('',(0.0577350269189626,-0.2,-0.1));
#10642=CARTESIAN_POINT('Origin',(-0.115470053837925,0.,-1.38777878078145E-17));
#10643=CARTESIAN_POINT('',(-0.115470053837925,0.,-1.41410031829988E-17));
#10644=CARTESIAN_POINT('',(-0.0797862971081845,0.,-0.0618060796608387));
#10645=CARTESIAN_POINT('',(-0.115470053837925,-0.2,-1.38777878078145E-17));
#10646=CARTESIAN_POINT('',(-0.115470053837925,0.,-1.41410031829988E-17));
#10647=CARTESIAN_POINT('',(-0.0577350269189626,-0.2,-0.1));
#10648=CARTESIAN_POINT('Origin',(-0.0577350269189626,0.,0.1));
#10649=CARTESIAN_POINT('',(-0.0577350269189626,0.,0.1));
#10650=CARTESIAN_POINT('',(-0.0509187836487033,0.,0.111806079660839));
#10651=CARTESIAN_POINT('',(-0.0577350269189626,-0.2,0.1));
#10652=CARTESIAN_POINT('',(-0.0577350269189626,0.,0.1));
#10653=CARTESIAN_POINT('',(-0.115470053837925,-0.2,-1.41410031829988E-17));
#10654=CARTESIAN_POINT('Origin',(0.0577350269189626,0.,0.1));
#10655=CARTESIAN_POINT('',(0.0577350269189626,0.,0.1));
#10656=CARTESIAN_POINT('',(0.113867513459481,0.,0.1));
#10657=CARTESIAN_POINT('',(0.0577350269189626,-0.2,0.1));
#10658=CARTESIAN_POINT('',(0.0577350269189626,0.,0.1));
#10659=CARTESIAN_POINT('',(-0.0577350269189626,-0.2,0.1));
#10660=CARTESIAN_POINT('Origin',(0.115470053837925,0.,0.));
#10661=CARTESIAN_POINT('',(0.122286297108185,0.,-0.0118060796608386));
#10662=CARTESIAN_POINT('',(0.0577350269189626,-0.2,0.1));
#10663=CARTESIAN_POINT('Origin',(0.,-0.2,0.));
#10664=CARTESIAN_POINT('Origin',(0.17,0.,0.));
#10665=CARTESIAN_POINT('',(-0.17,-8.67361737988404E-18,-2.0818995585505E-17));
#10666=CARTESIAN_POINT('Origin',(0.,0.,0.));
#10667=CARTESIAN_POINT('Origin',(0.,-0.015,0.));
#10668=CARTESIAN_POINT('',(-0.1954,-0.0254,-2.39295984553393E-17));
#10669=CARTESIAN_POINT('Origin',(0.,-0.0254,0.));
#10670=CARTESIAN_POINT('',(-0.185,-0.015,-2.2655965784226E-17));
#10671=CARTESIAN_POINT('Origin',(0.,-0.2775,0.));
#10672=CARTESIAN_POINT('',(-0.1954,-0.2775,-2.39295984553393E-17));
#11223=UNCERTAINTY_MEASURE_WITH_UNIT(LENGTH_MEASURE(0.001),#11259,
'DISTANCE_ACCURACY_VALUE',
'Maximum model space distance between geometric entities at asserted c
onnectivities');
#11228=UNCERTAINTY_MEASURE_WITH_UNIT(LENGTH_MEASURE(0.001),#11259,
'DISTANCE_ACCURACY_VALUE',
'Maximum model space distance between geometric entities at asserted c
onnectivities');
#11253=(
GEOMETRIC_REPRESENTATION_CONTEXT(3)
GLOBAL_UNCERTAINTY_ASSIGNED_CONTEXT((#11223))
GLOBAL_UNIT_ASSIGNED_CONTEXT((#11259,#11261,#11262))
REPRESENTATION_CONTEXT('','3D')
);
#11258=(
GEOMETRIC_REPRESENTATION_CONTEXT(3)
GLOBAL_UNCERTAINTY_ASSIGNED_CONTEXT((#11228))
GLOBAL_UNIT_ASSIGNED_CONTEXT((#11259,#11261,#11262))
REPRESENTATION_CONTEXT('','3D')
);
#11259=(
LENGTH_UNIT()
NAMED_UNIT(*)
SI_UNIT(.CENTI.,.METRE.)
);
#11261=(
NAMED_UNIT(*)
PLANE_ANGLE_UNIT()
SI_UNIT($,.RADIAN.)
);
#11262=(
NAMED_UNIT(*)
SI_UNIT($,.STERADIAN.)
SOLID_ANGLE_UNIT()
);
#11287=SHAPE_DEFINITION_REPRESENTATION(#11344,#11383);
#11344=PRODUCT_DEFINITION_SHAPE('',$,#11413);
#11383=SHAPE_REPRESENTATION('',(#5932),#11253);
#11388=PRODUCT_DEFINITION_CONTEXT('part definition',#11477,'design');
#11413=PRODUCT_DEFINITION('M4x4 collar screw','M4x4 collar screw',#11442,
#11388);
#11442=PRODUCT_DEFINITION_FORMATION('',$,#11503);
#11477=APPLICATION_CONTEXT(
'Core Data for Automotive Mechanical Design Process');
#11478=PRODUCT_CONTEXT('part definition',#11477,'mechanical');
#11503=PRODUCT('M4x4 collar screw','M4x4 collar screw',
'M4x4 collar screw',(#11478));
#11585=COLOUR_RGB('Black',0.12,0.14,0.17);
#11586=FILL_AREA_STYLE_COLOUR('',#11585);
#11587=FILL_AREA_STYLE('',(#11586));
#11588=SURFACE_STYLE_FILL_AREA(#11587);
#11589=SURFACE_SIDE_STYLE('',(#11588));
#11590=SURFACE_STYLE_USAGE(.BOTH.,#11589);
#11591=PRESENTATION_STYLE_ASSIGNMENT((#11590));
ENDSEC;
END-ISO-10303-21;
